ISO-10303-21;
HEADER;
/* Generated by software containing ST-Developer
 * from STEP Tools, Inc. (www.steptools.com) 
 */

FILE_DESCRIPTION(
/* description */ ('PAT-091'),
/* implementation_level */ '2;1');

FILE_NAME(
/* name */ 'Axle end keeper (2).step',
/* time_stamp */ '2026-10-27T15:34:44-07:00',
/* author */ (''),
/* organization */ (''),
/* preprocessor_version */ 'ST-DEVELOPER v20.2',
/* originating_system */ 'Autodesk Translation Framework v15.17.0.0',
/* authorisation */ '');

FILE_SCHEMA (('AUTOMOTIVE_DESIGN { 1 0 10303 214 3 1 1 }'));
ENDSEC;

DATA;
#10=MECHANICAL_DESIGN_GEOMETRIC_PRESENTATION_REPRESENTATION('',(#995),#25100);
#775=SHAPE_REPRESENTATION_RELATIONSHIP('SRR','None',#25537,#885);
#885=ADVANCED_BREP_SHAPE_REPRESENTATION('',(#1118),#25007);
#995=STYLED_ITEM('',(#26191),#1118);
#1118=MANIFOLD_SOLID_BREP('Body1',#13273);
#1379=FACE_BOUND('',#3267,.T.);
#1380=FACE_BOUND('',#3269,.T.);
#1754=PLANE('',#15045);
#1755=PLANE('',#15046);
#2282=FACE_OUTER_BOUND('',#3264,.T.);
#2283=FACE_OUTER_BOUND('',#3265,.T.);
#2284=FACE_OUTER_BOUND('',#3266,.T.);
#2285=FACE_OUTER_BOUND('',#3268,.T.);
#3264=EDGE_LOOP('',(#9920,#9921,#9922,#9923));
#3265=EDGE_LOOP('',(#9924,#9925,#9926,#9927));
#3266=EDGE_LOOP('',(#9928));
#3267=EDGE_LOOP('',(#9929));
#3268=EDGE_LOOP('',(#9930));
#3269=EDGE_LOOP('',(#9931));
#4391=LINE('',#22014,#5131);
#4392=LINE('',#22020,#5132);
#5131=VECTOR('',#17647,0.225);
#5132=VECTOR('',#17654,1.);
#5811=CIRCLE('',#15040,0.225);
#5812=CIRCLE('',#15041,0.225);
#5813=CIRCLE('',#15043,1.);
#5814=CIRCLE('',#15044,1.);
#6698=VERTEX_POINT('',#22011);
#6699=VERTEX_POINT('',#22013);
#6700=VERTEX_POINT('',#22017);
#6701=VERTEX_POINT('',#22019);
#7895=EDGE_CURVE('',#6698,#6698,#5811,.T.);
#7896=EDGE_CURVE('',#6698,#6699,#4391,.T.);
#7897=EDGE_CURVE('',#6699,#6699,#5812,.T.);
#7898=EDGE_CURVE('',#6700,#6700,#5813,.T.);
#7899=EDGE_CURVE('',#6700,#6701,#4392,.T.);
#7900=EDGE_CURVE('',#6701,#6701,#5814,.T.);
#9920=ORIENTED_EDGE('',*,*,#7895,.F.);
#9921=ORIENTED_EDGE('',*,*,#7896,.T.);
#9922=ORIENTED_EDGE('',*,*,#7897,.T.);
#9923=ORIENTED_EDGE('',*,*,#7896,.F.);
#9924=ORIENTED_EDGE('',*,*,#7898,.F.);
#9925=ORIENTED_EDGE('',*,*,#7899,.T.);
#9926=ORIENTED_EDGE('',*,*,#7900,.T.);
#9927=ORIENTED_EDGE('',*,*,#7899,.F.);
#9928=ORIENTED_EDGE('',*,*,#7898,.T.);
#9929=ORIENTED_EDGE('',*,*,#7895,.T.);
#9930=ORIENTED_EDGE('',*,*,#7900,.F.);
#9931=ORIENTED_EDGE('',*,*,#7897,.F.);
#12176=CYLINDRICAL_SURFACE('',#15039,0.225);
#12177=CYLINDRICAL_SURFACE('',#15042,1.);
#12649=ADVANCED_FACE('',(#2282),#12176,.F.);
#12650=ADVANCED_FACE('',(#2283),#12177,.T.);
#12651=ADVANCED_FACE('',(#2284,#1379),#1754,.T.);
#12652=ADVANCED_FACE('',(#2285,#1380),#1755,.F.);
#13273=CLOSED_SHELL('',(#12649,#12650,#12651,#12652));
#15038=AXIS2_PLACEMENT_3D('',#22009,#17641,#17642);
#15039=AXIS2_PLACEMENT_3D('',#22010,#17643,#17644);
#15040=AXIS2_PLACEMENT_3D('',#22012,#17645,#17646);
#15041=AXIS2_PLACEMENT_3D('',#22015,#17648,#17649);
#15042=AXIS2_PLACEMENT_3D('',#22016,#17650,#17651);
#15043=AXIS2_PLACEMENT_3D('',#22018,#17652,#17653);
#15044=AXIS2_PLACEMENT_3D('',#22021,#17655,#17656);
#15045=AXIS2_PLACEMENT_3D('',#22022,#17657,#17658);
#15046=AXIS2_PLACEMENT_3D('',#22023,#17659,#17660);
#17641=DIRECTION('axis',(0.,0.,1.));
#17642=DIRECTION('refdir',(1.,0.,0.));
#17643=DIRECTION('center_axis',(0.,1.,0.));
#17644=DIRECTION('ref_axis',(1.,0.,0.));
#17645=DIRECTION('center_axis',(0.,-1.,0.));
#17646=DIRECTION('ref_axis',(1.,0.,0.));
#17647=DIRECTION('',(0.,-1.,0.));
#17648=DIRECTION('center_axis',(0.,-1.,0.));
#17649=DIRECTION('ref_axis',(1.,0.,0.));
#17650=DIRECTION('center_axis',(0.,1.,0.));
#17651=DIRECTION('ref_axis',(1.,0.,0.));
#17652=DIRECTION('center_axis',(0.,1.,0.));
#17653=DIRECTION('ref_axis',(1.,0.,0.));
#17654=DIRECTION('',(0.,-1.,0.));
#17655=DIRECTION('center_axis',(0.,1.,0.));
#17656=DIRECTION('ref_axis',(1.,0.,0.));
#17657=DIRECTION('center_axis',(0.,1.,0.));
#17658=DIRECTION('ref_axis',(1.,0.,0.));
#17659=DIRECTION('center_axis',(0.,1.,0.));
#17660=DIRECTION('ref_axis',(1.,0.,0.));
#22009=CARTESIAN_POINT('',(0.,0.,0.));
#22010=CARTESIAN_POINT('Origin',(0.,-6.2,13.));
#22011=CARTESIAN_POINT('',(-0.225,-6.,13.));
#22012=CARTESIAN_POINT('Origin',(0.,-6.,13.));
#22013=CARTESIAN_POINT('',(-0.225,-6.2,13.));
#22014=CARTESIAN_POINT('',(-0.225,-6.2,13.));
#22015=CARTESIAN_POINT('Origin',(0.,-6.2,13.));
#22016=CARTESIAN_POINT('Origin',(0.,-6.2,13.));
#22017=CARTESIAN_POINT('',(-1.,-6.,13.));
#22018=CARTESIAN_POINT('Origin',(0.,-6.,13.));
#22019=CARTESIAN_POINT('',(-1.,-6.2,13.));
#22020=CARTESIAN_POINT('',(-1.,-6.2,13.));
#22021=CARTESIAN_POINT('Origin',(0.,-6.2,13.));
#22022=CARTESIAN_POINT('Origin',(0.,-6.,13.));
#22023=CARTESIAN_POINT('Origin',(0.,-6.2,13.));
#24886=UNCERTAINTY_MEASURE_WITH_UNIT(LENGTH_MEASURE(0.001),#25101,
'DISTANCE_ACCURACY_VALUE',
'Maximum model space distance between geometric entities at asserted c
onnectivities');
#24979=UNCERTAINTY_MEASURE_WITH_UNIT(LENGTH_MEASURE(0.001),#25101,
'DISTANCE_ACCURACY_VALUE',
'Maximum model space distance between geometric entities at asserted c
onnectivities');
#25007=(
GEOMETRIC_REPRESENTATION_CONTEXT(3)
GLOBAL_UNCERTAINTY_ASSIGNED_CONTEXT((#24886))
GLOBAL_UNIT_ASSIGNED_CONTEXT((#25101,#25103,#25104))
REPRESENTATION_CONTEXT('','3D')
);
#25100=(
GEOMETRIC_REPRESENTATION_CONTEXT(3)
GLOBAL_UNCERTAINTY_ASSIGNED_CONTEXT((#24979))
GLOBAL_UNIT_ASSIGNED_CONTEXT((#25101,#25103,#25104))
REPRESENTATION_CONTEXT('','3D')
);
#25101=(
LENGTH_UNIT()
NAMED_UNIT(*)
SI_UNIT(.CENTI.,.METRE.)
);
#25103=(
NAMED_UNIT(*)
PLANE_ANGLE_UNIT()
SI_UNIT($,.RADIAN.)
);
#25104=(
NAMED_UNIT(*)
SI_UNIT($,.STERADIAN.)
SOLID_ANGLE_UNIT()
);
#25132=SHAPE_DEFINITION_REPRESENTATION(#25252,#25537);
#25252=PRODUCT_DEFINITION_SHAPE('',$,#25658);
#25537=SHAPE_REPRESENTATION('',(#15038),#25007);
#25630=PRODUCT_DEFINITION_CONTEXT('part definition',#25992,'design');
#25658=PRODUCT_DEFINITION('Axle end keeper (2)','Axle end keeper (2)',#25778,
#25630);
#25778=PRODUCT_DEFINITION_FORMATION('',$,#26021);
#25992=APPLICATION_CONTEXT(
'Core Data for Automotive Mechanical Design Process');
#25993=PRODUCT_CONTEXT('part definition',#25992,'mechanical');
#26021=PRODUCT('Axle end keeper (2)','Axle end keeper (2)',
'Axle end keeper (2)',(#25993));
#26185=COLOUR_RGB('Grey',0.48,0.52,0.57);
#26186=FILL_AREA_STYLE_COLOUR('',#26185);
#26187=FILL_AREA_STYLE('',(#26186));
#26188=SURFACE_STYLE_FILL_AREA(#26187);
#26189=SURFACE_SIDE_STYLE('',(#26188));
#26190=SURFACE_STYLE_USAGE(.BOTH.,#26189);
#26191=PRESENTATION_STYLE_ASSIGNMENT((#26190));
ENDSEC;
END-ISO-10303-21;
